ISO-10303-21;
HEADER;
/* Generated by software containing ST-Developer
 * from STEP Tools, Inc. (www.steptools.com) 
 */

FILE_DESCRIPTION(
/* description */ ('Self-centering screw clamp'),
/* implementation_level */ '2;1');

FILE_NAME(
/* name */ 'Opposed M12 x 3 screw envelope.step',
/* time_stamp */ '2026-10-28T03:25:31-07:00',
/* author */ (''),
/* organization */ (''),
/* preprocessor_version */ 'ST-DEVELOPER v20.2',
/* originating_system */ 'Autodesk Translation Framework v15.17.0.0',
/* authorisation */ '');

FILE_SCHEMA (('AUTOMOTIVE_DESIGN { 1 0 10303 214 3 1 1 }'));
ENDSEC;

DATA;
#10=MECHANICAL_DESIGN_GEOMETRIC_PRESENTATION_REPRESENTATION('',(#663),#16799);
#574=SHAPE_REPRESENTATION_RELATIONSHIP('SRR','None',#17052,#615);
#615=ADVANCED_BREP_SHAPE_REPRESENTATION('',(#710),#16790);
#663=STYLED_ITEM('',(#17333),#710);
#710=MANIFOLD_SOLID_BREP('Body1',#9115);
#993=FACE_BOUND('',#2485,.T.);
#994=FACE_BOUND('',#2487,.T.);
#995=FACE_BOUND('',#2491,.T.);
#996=FACE_BOUND('',#2493,.T.);
#997=FACE_BOUND('',#2498,.T.);
#998=FACE_BOUND('',#2500,.T.);
#1228=PLANE('',#10509);
#1229=PLANE('',#10513);
#1230=PLANE('',#10514);
#1231=PLANE('',#10517);
#1232=PLANE('',#10523);
#1233=PLANE('',#10525);
#1234=PLANE('',#10533);
#1235=PLANE('',#10534);
#1701=FACE_OUTER_BOUND('',#2480,.T.);
#1702=FACE_OUTER_BOUND('',#2481,.T.);
#1703=FACE_OUTER_BOUND('',#2482,.T.);
#1704=FACE_OUTER_BOUND('',#2483,.T.);
#1705=FACE_OUTER_BOUND('',#2484,.T.);
#1706=FACE_OUTER_BOUND('',#2486,.T.);
#1707=FACE_OUTER_BOUND('',#2488,.T.);
#1708=FACE_OUTER_BOUND('',#2489,.T.);
#1709=FACE_OUTER_BOUND('',#2490,.T.);
#1710=FACE_OUTER_BOUND('',#2492,.T.);
#1711=FACE_OUTER_BOUND('',#2494,.T.);
#1712=FACE_OUTER_BOUND('',#2495,.T.);
#1713=FACE_OUTER_BOUND('',#2496,.T.);
#1714=FACE_OUTER_BOUND('',#2497,.T.);
#1715=FACE_OUTER_BOUND('',#2499,.T.);
#2480=EDGE_LOOP('',(#8067,#8068,#8069,#8070));
#2481=EDGE_LOOP('',(#8071));
#2482=EDGE_LOOP('',(#8072,#8073,#8074,#8075));
#2483=EDGE_LOOP('',(#8076));
#2484=EDGE_LOOP('',(#8077));
#2485=EDGE_LOOP('',(#8078));
#2486=EDGE_LOOP('',(#8079));
#2487=EDGE_LOOP('',(#8080));
#2488=EDGE_LOOP('',(#8081,#8082,#8083,#8084));
#2489=EDGE_LOOP('',(#8085,#8086,#8087,#8088));
#2490=EDGE_LOOP('',(#8089));
#2491=EDGE_LOOP('',(#8090));
#2492=EDGE_LOOP('',(#8091));
#2493=EDGE_LOOP('',(#8092));
#2494=EDGE_LOOP('',(#8093,#8094,#8095,#8096));
#2495=EDGE_LOOP('',(#8097,#8098,#8099,#8100));
#2496=EDGE_LOOP('',(#8101,#8102,#8103,#8104));
#2497=EDGE_LOOP('',(#8105));
#2498=EDGE_LOOP('',(#8106));
#2499=EDGE_LOOP('',(#8107));
#2500=EDGE_LOOP('',(#8108));
#3075=LINE('',#16159,#3648);
#3076=LINE('',#16166,#3649);
#3077=LINE('',#16180,#3650);
#3078=LINE('',#16183,#3651);
#3079=LINE('',#16194,#3652);
#3080=LINE('',#16197,#3653);
#3081=LINE('',#16202,#3654);
#3648=VECTOR('',#13112,0.165);
#3649=VECTOR('',#13121,0.165);
#3650=VECTOR('',#13140,0.8);
#3651=VECTOR('',#13143,0.6);
#3652=VECTOR('',#13158,0.8);
#3653=VECTOR('',#13161,0.6);
#3654=VECTOR('',#13168,0.6);
#4177=CIRCLE('',#10507,0.165);
#4178=CIRCLE('',#10508,0.165);
#4179=CIRCLE('',#10511,0.165);
#4180=CIRCLE('',#10512,0.165);
#4181=CIRCLE('',#10515,0.8);
#4182=CIRCLE('',#10516,0.6);
#4183=CIRCLE('',#10518,0.8);
#4184=CIRCLE('',#10519,0.6);
#4185=CIRCLE('',#10522,0.6);
#4186=CIRCLE('',#10524,0.8);
#4187=CIRCLE('',#10526,0.8);
#4188=CIRCLE('',#10527,0.6);
#4189=CIRCLE('',#10530,0.6);
#4190=CIRCLE('',#10532,0.6);
#4882=VERTEX_POINT('',#16156);
#4883=VERTEX_POINT('',#16158);
#4884=VERTEX_POINT('',#16163);
#4885=VERTEX_POINT('',#16165);
#4886=VERTEX_POINT('',#16170);
#4887=VERTEX_POINT('',#16172);
#4888=VERTEX_POINT('',#16175);
#4889=VERTEX_POINT('',#16177);
#4890=VERTEX_POINT('',#16182);
#4891=VERTEX_POINT('',#16186);
#4892=VERTEX_POINT('',#16189);
#4893=VERTEX_POINT('',#16191);
#4894=VERTEX_POINT('',#16196);
#4895=VERTEX_POINT('',#16200);
#5958=EDGE_CURVE('',#4882,#4882,#4177,.T.);
#5959=EDGE_CURVE('',#4882,#4883,#3075,.T.);
#5960=EDGE_CURVE('',#4883,#4883,#4178,.T.);
#5961=EDGE_CURVE('',#4884,#4884,#4179,.T.);
#5962=EDGE_CURVE('',#4884,#4885,#3076,.T.);
#5963=EDGE_CURVE('',#4885,#4885,#4180,.T.);
#5964=EDGE_CURVE('',#4886,#4886,#4181,.T.);
#5965=EDGE_CURVE('',#4887,#4887,#4182,.T.);
#5966=EDGE_CURVE('',#4888,#4888,#4183,.T.);
#5967=EDGE_CURVE('',#4889,#4889,#4184,.T.);
#5968=EDGE_CURVE('',#4886,#4888,#3077,.T.);
#5969=EDGE_CURVE('',#4889,#4890,#3078,.T.);
#5970=EDGE_CURVE('',#4890,#4890,#4185,.T.);
#5971=EDGE_CURVE('',#4891,#4891,#4186,.T.);
#5972=EDGE_CURVE('',#4892,#4892,#4187,.T.);
#5973=EDGE_CURVE('',#4893,#4893,#4188,.T.);
#5974=EDGE_CURVE('',#4891,#4892,#3079,.T.);
#5975=EDGE_CURVE('',#4893,#4894,#3080,.T.);
#5976=EDGE_CURVE('',#4894,#4894,#4189,.T.);
#5977=EDGE_CURVE('',#4895,#4895,#4190,.T.);
#5978=EDGE_CURVE('',#4895,#4887,#3081,.T.);
#8067=ORIENTED_EDGE('',*,*,#5958,.F.);
#8068=ORIENTED_EDGE('',*,*,#5959,.T.);
#8069=ORIENTED_EDGE('',*,*,#5960,.F.);
#8070=ORIENTED_EDGE('',*,*,#5959,.F.);
#8071=ORIENTED_EDGE('',*,*,#5958,.T.);
#8072=ORIENTED_EDGE('',*,*,#5961,.F.);
#8073=ORIENTED_EDGE('',*,*,#5962,.T.);
#8074=ORIENTED_EDGE('',*,*,#5963,.T.);
#8075=ORIENTED_EDGE('',*,*,#5962,.F.);
#8076=ORIENTED_EDGE('',*,*,#5963,.F.);
#8077=ORIENTED_EDGE('',*,*,#5964,.T.);
#8078=ORIENTED_EDGE('',*,*,#5965,.F.);
#8079=ORIENTED_EDGE('',*,*,#5966,.F.);
#8080=ORIENTED_EDGE('',*,*,#5967,.F.);
#8081=ORIENTED_EDGE('',*,*,#5964,.F.);
#8082=ORIENTED_EDGE('',*,*,#5968,.T.);
#8083=ORIENTED_EDGE('',*,*,#5966,.T.);
#8084=ORIENTED_EDGE('',*,*,#5968,.F.);
#8085=ORIENTED_EDGE('',*,*,#5967,.T.);
#8086=ORIENTED_EDGE('',*,*,#5969,.T.);
#8087=ORIENTED_EDGE('',*,*,#5970,.T.);
#8088=ORIENTED_EDGE('',*,*,#5969,.F.);
#8089=ORIENTED_EDGE('',*,*,#5971,.T.);
#8090=ORIENTED_EDGE('',*,*,#5970,.F.);
#8091=ORIENTED_EDGE('',*,*,#5972,.F.);
#8092=ORIENTED_EDGE('',*,*,#5973,.F.);
#8093=ORIENTED_EDGE('',*,*,#5971,.F.);
#8094=ORIENTED_EDGE('',*,*,#5974,.T.);
#8095=ORIENTED_EDGE('',*,*,#5972,.T.);
#8096=ORIENTED_EDGE('',*,*,#5974,.F.);
#8097=ORIENTED_EDGE('',*,*,#5973,.T.);
#8098=ORIENTED_EDGE('',*,*,#5975,.T.);
#8099=ORIENTED_EDGE('',*,*,#5976,.T.);
#8100=ORIENTED_EDGE('',*,*,#5975,.F.);
#8101=ORIENTED_EDGE('',*,*,#5977,.F.);
#8102=ORIENTED_EDGE('',*,*,#5978,.T.);
#8103=ORIENTED_EDGE('',*,*,#5965,.T.);
#8104=ORIENTED_EDGE('',*,*,#5978,.F.);
#8105=ORIENTED_EDGE('',*,*,#5977,.T.);
#8106=ORIENTED_EDGE('',*,*,#5960,.T.);
#8107=ORIENTED_EDGE('',*,*,#5976,.F.);
#8108=ORIENTED_EDGE('',*,*,#5961,.T.);
#8546=CYLINDRICAL_SURFACE('',#10506,0.165);
#8547=CYLINDRICAL_SURFACE('',#10510,0.165);
#8548=CYLINDRICAL_SURFACE('',#10520,0.8);
#8549=CYLINDRICAL_SURFACE('',#10521,0.6);
#8550=CYLINDRICAL_SURFACE('',#10528,0.8);
#8551=CYLINDRICAL_SURFACE('',#10529,0.6);
#8552=CYLINDRICAL_SURFACE('',#10531,0.6);
#8999=ADVANCED_FACE('',(#1701),#8546,.F.);
#9000=ADVANCED_FACE('',(#1702),#1228,.T.);
#9001=ADVANCED_FACE('',(#1703),#8547,.F.);
#9002=ADVANCED_FACE('',(#1704),#1229,.F.);
#9003=ADVANCED_FACE('',(#1705,#993),#1230,.T.);
#9004=ADVANCED_FACE('',(#1706,#994),#1231,.F.);
#9005=ADVANCED_FACE('',(#1707),#8548,.T.);
#9006=ADVANCED_FACE('',(#1708),#8549,.T.);
#9007=ADVANCED_FACE('',(#1709,#995),#1232,.T.);
#9008=ADVANCED_FACE('',(#1710,#996),#1233,.F.);
#9009=ADVANCED_FACE('',(#1711),#8550,.T.);
#9010=ADVANCED_FACE('',(#1712),#8551,.T.);
#9011=ADVANCED_FACE('',(#1713),#8552,.T.);
#9012=ADVANCED_FACE('',(#1714,#997),#1234,.T.);
#9013=ADVANCED_FACE('',(#1715,#998),#1235,.F.);
#9115=CLOSED_SHELL('',(#8999,#9000,#9001,#9002,#9003,#9004,#9005,#9006,
#9007,#9008,#9009,#9010,#9011,#9012,#9013));
#10505=AXIS2_PLACEMENT_3D('',#16154,#13106,#13107);
#10506=AXIS2_PLACEMENT_3D('',#16155,#13108,#13109);
#10507=AXIS2_PLACEMENT_3D('',#16157,#13110,#13111);
#10508=AXIS2_PLACEMENT_3D('',#16160,#13113,#13114);
#10509=AXIS2_PLACEMENT_3D('',#16161,#13115,#13116);
#10510=AXIS2_PLACEMENT_3D('',#16162,#13117,#13118);
#10511=AXIS2_PLACEMENT_3D('',#16164,#13119,#13120);
#10512=AXIS2_PLACEMENT_3D('',#16167,#13122,#13123);
#10513=AXIS2_PLACEMENT_3D('',#16168,#13124,#13125);
#10514=AXIS2_PLACEMENT_3D('',#16169,#13126,#13127);
#10515=AXIS2_PLACEMENT_3D('',#16171,#13128,#13129);
#10516=AXIS2_PLACEMENT_3D('',#16173,#13130,#13131);
#10517=AXIS2_PLACEMENT_3D('',#16174,#13132,#13133);
#10518=AXIS2_PLACEMENT_3D('',#16176,#13134,#13135);
#10519=AXIS2_PLACEMENT_3D('',#16178,#13136,#13137);
#10520=AXIS2_PLACEMENT_3D('',#16179,#13138,#13139);
#10521=AXIS2_PLACEMENT_3D('',#16181,#13141,#13142);
#10522=AXIS2_PLACEMENT_3D('',#16184,#13144,#13145);
#10523=AXIS2_PLACEMENT_3D('',#16185,#13146,#13147);
#10524=AXIS2_PLACEMENT_3D('',#16187,#13148,#13149);
#10525=AXIS2_PLACEMENT_3D('',#16188,#13150,#13151);
#10526=AXIS2_PLACEMENT_3D('',#16190,#13152,#13153);
#10527=AXIS2_PLACEMENT_3D('',#16192,#13154,#13155);
#10528=AXIS2_PLACEMENT_3D('',#16193,#13156,#13157);
#10529=AXIS2_PLACEMENT_3D('',#16195,#13159,#13160);
#10530=AXIS2_PLACEMENT_3D('',#16198,#13162,#13163);
#10531=AXIS2_PLACEMENT_3D('',#16199,#13164,#13165);
#10532=AXIS2_PLACEMENT_3D('',#16201,#13166,#13167);
#10533=AXIS2_PLACEMENT_3D('',#16203,#13169,#13170);
#10534=AXIS2_PLACEMENT_3D('',#16204,#13171,#13172);
#13106=DIRECTION('axis',(0.,0.,1.));
#13107=DIRECTION('refdir',(1.,0.,0.));
#13108=DIRECTION('center_axis',(1.,0.,0.));
#13109=DIRECTION('ref_axis',(0.,0.,-1.));
#13110=DIRECTION('center_axis',(1.,0.,0.));
#13111=DIRECTION('ref_axis',(0.,0.,-1.));
#13112=DIRECTION('',(1.,0.,0.));
#13113=DIRECTION('center_axis',(-1.,0.,0.));
#13114=DIRECTION('ref_axis',(0.,0.,-1.));
#13115=DIRECTION('center_axis',(1.,0.,0.));
#13116=DIRECTION('ref_axis',(0.,0.,-1.));
#13117=DIRECTION('center_axis',(1.,0.,0.));
#13118=DIRECTION('ref_axis',(0.,0.,-1.));
#13119=DIRECTION('center_axis',(1.,0.,0.));
#13120=DIRECTION('ref_axis',(0.,0.,-1.));
#13121=DIRECTION('',(1.,0.,0.));
#13122=DIRECTION('center_axis',(1.,0.,0.));
#13123=DIRECTION('ref_axis',(0.,0.,-1.));
#13124=DIRECTION('center_axis',(1.,0.,0.));
#13125=DIRECTION('ref_axis',(0.,0.,-1.));
#13126=DIRECTION('center_axis',(1.,0.,0.));
#13127=DIRECTION('ref_axis',(0.,0.,-1.));
#13128=DIRECTION('center_axis',(1.,0.,0.));
#13129=DIRECTION('ref_axis',(0.,0.,-1.));
#13130=DIRECTION('center_axis',(1.,0.,0.));
#13131=DIRECTION('ref_axis',(0.,0.,-1.));
#13132=DIRECTION('center_axis',(1.,0.,0.));
#13133=DIRECTION('ref_axis',(0.,0.,-1.));
#13134=DIRECTION('center_axis',(1.,0.,0.));
#13135=DIRECTION('ref_axis',(0.,0.,-1.));
#13136=DIRECTION('center_axis',(-1.,0.,0.));
#13137=DIRECTION('ref_axis',(0.,0.,-1.));
#13138=DIRECTION('center_axis',(1.,0.,0.));
#13139=DIRECTION('ref_axis',(0.,0.,-1.));
#13140=DIRECTION('',(-1.,0.,0.));
#13141=DIRECTION('center_axis',(1.,0.,0.));
#13142=DIRECTION('ref_axis',(0.,0.,-1.));
#13143=DIRECTION('',(-1.,0.,0.));
#13144=DIRECTION('center_axis',(1.,0.,0.));
#13145=DIRECTION('ref_axis',(0.,0.,-1.));
#13146=DIRECTION('center_axis',(1.,0.,0.));
#13147=DIRECTION('ref_axis',(0.,0.,-1.));
#13148=DIRECTION('center_axis',(1.,0.,0.));
#13149=DIRECTION('ref_axis',(0.,0.,-1.));
#13150=DIRECTION('center_axis',(1.,0.,0.));
#13151=DIRECTION('ref_axis',(0.,0.,-1.));
#13152=DIRECTION('center_axis',(1.,0.,0.));
#13153=DIRECTION('ref_axis',(0.,0.,-1.));
#13154=DIRECTION('center_axis',(-1.,0.,0.));
#13155=DIRECTION('ref_axis',(0.,0.,-1.));
#13156=DIRECTION('center_axis',(1.,0.,0.));
#13157=DIRECTION('ref_axis',(0.,0.,-1.));
#13158=DIRECTION('',(-1.,0.,0.));
#13159=DIRECTION('center_axis',(1.,0.,0.));
#13160=DIRECTION('ref_axis',(0.,0.,-1.));
#13161=DIRECTION('',(-1.,0.,0.));
#13162=DIRECTION('center_axis',(1.,0.,0.));
#13163=DIRECTION('ref_axis',(0.,0.,-1.));
#13164=DIRECTION('center_axis',(1.,0.,0.));
#13165=DIRECTION('ref_axis',(0.,0.,-1.));
#13166=DIRECTION('center_axis',(1.,0.,0.));
#13167=DIRECTION('ref_axis',(0.,0.,-1.));
#13168=DIRECTION('',(-1.,0.,0.));
#13169=DIRECTION('center_axis',(1.,0.,0.));
#13170=DIRECTION('ref_axis',(0.,0.,-1.));
#13171=DIRECTION('center_axis',(1.,0.,0.));
#13172=DIRECTION('ref_axis',(0.,0.,-1.));
#16154=CARTESIAN_POINT('',(0.,0.,0.));
#16155=CARTESIAN_POINT('Origin',(13.,0.,4.));
#16156=CARTESIAN_POINT('',(13.,-2.02066721859313E-17,4.165));
#16157=CARTESIAN_POINT('Origin',(13.,0.,4.));
#16158=CARTESIAN_POINT('',(14.5,2.02066721859313E-17,4.165));
#16159=CARTESIAN_POINT('',(13.,-2.02066721859313E-17,4.165));
#16160=CARTESIAN_POINT('Origin',(14.5,0.,4.));
#16161=CARTESIAN_POINT('Origin',(13.,0.,4.));
#16162=CARTESIAN_POINT('Origin',(-15.1,0.,4.));
#16163=CARTESIAN_POINT('',(-15.,-2.02066721859313E-17,4.165));
#16164=CARTESIAN_POINT('Origin',(-15.,0.,4.));
#16165=CARTESIAN_POINT('',(-13.4,-2.02066721859313E-17,4.165));
#16166=CARTESIAN_POINT('',(-15.1,-2.02066721859313E-17,4.165));
#16167=CARTESIAN_POINT('Origin',(-13.4,0.,4.));
#16168=CARTESIAN_POINT('Origin',(-13.4,0.,4.));
#16169=CARTESIAN_POINT('Origin',(11.,0.,4.));
#16170=CARTESIAN_POINT('',(11.,-9.79717439317882E-17,4.8));
#16171=CARTESIAN_POINT('Origin',(11.,0.,4.));
#16172=CARTESIAN_POINT('',(11.,-7.34788079488412E-17,4.6));
#16173=CARTESIAN_POINT('Origin',(11.,0.,4.));
#16174=CARTESIAN_POINT('Origin',(10.,0.,4.));
#16175=CARTESIAN_POINT('',(10.,-9.79717439317882E-17,4.8));
#16176=CARTESIAN_POINT('Origin',(10.,0.,4.));
#16177=CARTESIAN_POINT('',(10.,7.34788079488412E-17,4.6));
#16178=CARTESIAN_POINT('Origin',(10.,0.,4.));
#16179=CARTESIAN_POINT('Origin',(10.,0.,4.));
#16180=CARTESIAN_POINT('',(10.,-9.79717439317882E-17,4.8));
#16181=CARTESIAN_POINT('Origin',(-15.,0.,4.));
#16182=CARTESIAN_POINT('',(-10.,-7.34788079488412E-17,4.6));
#16183=CARTESIAN_POINT('',(-15.,-7.34788079488412E-17,4.6));
#16184=CARTESIAN_POINT('Origin',(-10.,0.,4.));
#16185=CARTESIAN_POINT('Origin',(-10.,0.,4.));
#16186=CARTESIAN_POINT('',(-10.,-9.79717439317882E-17,4.8));
#16187=CARTESIAN_POINT('Origin',(-10.,0.,4.));
#16188=CARTESIAN_POINT('Origin',(-11.,0.,4.));
#16189=CARTESIAN_POINT('',(-11.,-9.79717439317882E-17,4.8));
#16190=CARTESIAN_POINT('Origin',(-11.,0.,4.));
#16191=CARTESIAN_POINT('',(-11.,7.34788079488412E-17,4.6));
#16192=CARTESIAN_POINT('Origin',(-11.,0.,4.));
#16193=CARTESIAN_POINT('Origin',(-11.,0.,4.));
#16194=CARTESIAN_POINT('',(-11.,-9.79717439317882E-17,4.8));
#16195=CARTESIAN_POINT('Origin',(-15.,0.,4.));
#16196=CARTESIAN_POINT('',(-15.,-7.34788079488412E-17,4.6));
#16197=CARTESIAN_POINT('',(-15.,-7.34788079488412E-17,4.6));
#16198=CARTESIAN_POINT('Origin',(-15.,0.,4.));
#16199=CARTESIAN_POINT('Origin',(-15.,0.,4.));
#16200=CARTESIAN_POINT('',(14.5,-7.34788079488412E-17,4.6));
#16201=CARTESIAN_POINT('Origin',(14.5,0.,4.));
#16202=CARTESIAN_POINT('',(-15.,-7.34788079488412E-17,4.6));
#16203=CARTESIAN_POINT('Origin',(14.5,0.,4.));
#16204=CARTESIAN_POINT('Origin',(-15.,0.,4.));
#16741=UNCERTAINTY_MEASURE_WITH_UNIT(LENGTH_MEASURE(0.001),#16800,
'DISTANCE_ACCURACY_VALUE',
'Maximum model space distance between geometric entities at asserted c
onnectivities');
#16750=UNCERTAINTY_MEASURE_WITH_UNIT(LENGTH_MEASURE(0.001),#16800,
'DISTANCE_ACCURACY_VALUE',
'Maximum model space distance between geometric entities at asserted c
onnectivities');
#16790=(
GEOMETRIC_REPRESENTATION_CONTEXT(3)
GLOBAL_UNCERTAINTY_ASSIGNED_CONTEXT((#16741))
GLOBAL_UNIT_ASSIGNED_CONTEXT((#16800,#16802,#16803))
REPRESENTATION_CONTEXT('','3D')
);
#16799=(
GEOMETRIC_REPRESENTATION_CONTEXT(3)
GLOBAL_UNCERTAINTY_ASSIGNED_CONTEXT((#16750))
GLOBAL_UNIT_ASSIGNED_CONTEXT((#16800,#16802,#16803))
REPRESENTATION_CONTEXT('','3D')
);
#16800=(
LENGTH_UNIT()
NAMED_UNIT(*)
SI_UNIT(.CENTI.,.METRE.)
);
#16802=(
NAMED_UNIT(*)
PLANE_ANGLE_UNIT()
SI_UNIT($,.RADIAN.)
);
#16803=(
NAMED_UNIT(*)
SI_UNIT($,.STERADIAN.)
SOLID_ANGLE_UNIT()
);
#16843=SHAPE_DEFINITION_REPRESENTATION(#16898,#17052);
#16898=PRODUCT_DEFINITION_SHAPE('',$,#17101);
#17052=SHAPE_REPRESENTATION('',(#10505),#16790);
#17061=PRODUCT_DEFINITION_CONTEXT('part definition',#17207,'design');
#17101=PRODUCT_DEFINITION('Opposed M12 x 3 screw envelope',
'Opposed M12 x 3 screw envelope',#17149,#17061);
#17149=PRODUCT_DEFINITION_FORMATION('',$,#17248);
#17207=APPLICATION_CONTEXT(
'Core Data for Automotive Mechanical Design Process');
#17208=PRODUCT_CONTEXT('part definition',#17207,'mechanical');
#17248=PRODUCT('Opposed M12 x 3 screw envelope',
'Opposed M12 x 3 screw envelope','Opposed M12 x 3 screw envelope',(#17208));
#17327=COLOUR_RGB('Black',0.12,0.14,0.17);
#17328=FILL_AREA_STYLE_COLOUR('',#17327);
#17329=FILL_AREA_STYLE('',(#17328));
#17330=SURFACE_STYLE_FILL_AREA(#17329);
#17331=SURFACE_SIDE_STYLE('',(#17330));
#17332=SURFACE_STYLE_USAGE(.BOTH.,#17331);
#17333=PRESENTATION_STYLE_ASSIGNMENT((#17332));
ENDSEC;
END-ISO-10303-21;
